ISO-10303-21;
HEADER;
/* Generated by software containing ST-Developer
 * from STEP Tools, Inc. (www.steptools.com) 
 */

FILE_DESCRIPTION(
/* description */ (''),
/* implementation_level */ '2;1');

FILE_NAME(
/* name */ 'M5x14 Steel 4.6 Plain v1 (2).step',
/* time_stamp */ '2026-10-23T22:29:29+06:00',
/* author */ (''),
/* organization */ (''),
/* preprocessor_version */ 'ST-DEVELOPER v20.2',
/* originating_system */ 'Autodesk Translation Framework v15.15.0.0',
/* authorisation */ '');

FILE_SCHEMA (('AUTOMOTIVE_DESIGN { 1 0 10303 214 3 1 1 }'));
ENDSEC;

DATA;
#10=MECHANICAL_DESIGN_GEOMETRIC_PRESENTATION_REPRESENTATION('',(#74),#7047);
#54=SHAPE_REPRESENTATION_RELATIONSHIP('SRR','None',#7087,#64);
#64=ADVANCED_BREP_SHAPE_REPRESENTATION('',(#87),#7039);
#74=STYLED_ITEM('',(#7212),#87);
#87=MANIFOLD_SOLID_BREP('Body1',#3399);
#97=SPHERICAL_SURFACE('',#3697,12.8319377609308);
#103=CONICAL_SURFACE('',#3692,2.33923048454133,0.261799387799147);
#104=CONICAL_SURFACE('',#3701,5.05813690328693,0.0872664626099692);
#109=FACE_BOUND('',#526,.T.);
#127=TOROIDAL_SURFACE('',#3684,2.37846096908266,0.2);
#159=PLANE('',#3646);
#160=PLANE('',#3648);
#161=PLANE('',#3651);
#162=PLANE('',#3656);
#163=PLANE('',#3658);
#164=PLANE('',#3661);
#165=PLANE('',#3667);
#166=PLANE('',#3672);
#167=PLANE('',#3674);
#168=PLANE('',#3676);
#169=PLANE('',#3679);
#170=PLANE('',#3681);
#171=PLANE('',#3683);
#172=PLANE('',#3688);
#173=PLANE('',#3696);
#316=FACE_OUTER_BOUND('',#507,.T.);
#317=FACE_OUTER_BOUND('',#508,.T.);
#318=FACE_OUTER_BOUND('',#509,.T.);
#319=FACE_OUTER_BOUND('',#510,.T.);
#320=FACE_OUTER_BOUND('',#511,.T.);
#321=FACE_OUTER_BOUND('',#512,.T.);
#322=FACE_OUTER_BOUND('',#513,.T.);
#323=FACE_OUTER_BOUND('',#514,.T.);
#324=FACE_OUTER_BOUND('',#515,.T.);
#325=FACE_OUTER_BOUND('',#516,.T.);
#326=FACE_OUTER_BOUND('',#517,.T.);
#327=FACE_OUTER_BOUND('',#518,.T.);
#328=FACE_OUTER_BOUND('',#519,.T.);
#329=FACE_OUTER_BOUND('',#520,.T.);
#330=FACE_OUTER_BOUND('',#521,.T.);
#331=FACE_OUTER_BOUND('',#522,.T.);
#332=FACE_OUTER_BOUND('',#523,.T.);
#333=FACE_OUTER_BOUND('',#524,.T.);
#334=FACE_OUTER_BOUND('',#525,.T.);
#335=FACE_OUTER_BOUND('',#527,.T.);
#336=FACE_OUTER_BOUND('',#528,.T.);
#337=FACE_OUTER_BOUND('',#529,.T.);
#338=FACE_OUTER_BOUND('',#530,.T.);
#339=FACE_OUTER_BOUND('',#531,.T.);
#340=FACE_OUTER_BOUND('',#532,.T.);
#507=EDGE_LOOP('',(#2473,#2474,#2475,#2476,#2477,#2478));
#508=EDGE_LOOP('',(#2479,#2480,#2481));
#509=EDGE_LOOP('',(#2482,#2483,#2484,#2485,#2486,#2487));
#510=EDGE_LOOP('',(#2488,#2489,#2490));
#511=EDGE_LOOP('',(#2491,#2492,#2493,#2494,#2495,#2496));
#512=EDGE_LOOP('',(#2497,#2498,#2499));
#513=EDGE_LOOP('',(#2500,#2501,#2502,#2503,#2504,#2505));
#514=EDGE_LOOP('',(#2506,#2507,#2508));
#515=EDGE_LOOP('',(#2509,#2510,#2511,#2512,#2513,#2514));
#516=EDGE_LOOP('',(#2515,#2516,#2517));
#517=EDGE_LOOP('',(#2518,#2519,#2520,#2521,#2522,#2523));
#518=EDGE_LOOP('',(#2524,#2525,#2526));
#519=EDGE_LOOP('',(#2527,#2528,#2529));
#520=EDGE_LOOP('',(#2530,#2531,#2532,#2533,#2534,#2535,#2536));
#521=EDGE_LOOP('',(#2537,#2538,#2539));
#522=EDGE_LOOP('',(#2540,#2541,#2542,#2543,#2544,#2545));
#523=EDGE_LOOP('',(#2546,#2547,#2548,#2549,#2550,#2551,#2552,#2553));
#524=EDGE_LOOP('',(#2554,#2555,#2556,#2557));
#525=EDGE_LOOP('',(#2558));
#526=EDGE_LOOP('',(#2559));
#527=EDGE_LOOP('',(#2560,#2561,#2562,#2563));
#528=EDGE_LOOP('',(#2564,#2565,#2566,#2567));
#529=EDGE_LOOP('',(#2568,#2569,#2570,#2571));
#530=EDGE_LOOP('',(#2572));
#531=EDGE_LOOP('',(#2573,#2574,#2575,#2576,#2577,#2578,#2579,#2580,#2581,
#2582,#2583,#2584,#2585,#2586,#2587,#2588,#2589,#2590,#2591,#2592,#2593));
#532=EDGE_LOOP('',(#2594,#2595,#2596,#2597,#2598));
#716=CIRCLE('',#3644,0.946);
#717=CIRCLE('',#3647,12.8232171353527);
#718=CIRCLE('',#3649,12.1073709048319);
#719=CIRCLE('',#3652,12.8232171353527);
#720=CIRCLE('',#3654,0.946);
#721=CIRCLE('',#3657,12.8232171353527);
#722=CIRCLE('',#3659,12.1073709048319);
#723=CIRCLE('',#3662,12.8232171353527);
#724=CIRCLE('',#3665,0.946);
#725=CIRCLE('',#3668,12.8232171353527);
#726=CIRCLE('',#3670,0.946);
#727=CIRCLE('',#3673,12.8232171353527);
#728=CIRCLE('',#3675,12.8232171353527);
#729=CIRCLE('',#3677,12.1073709048319);
#730=CIRCLE('',#3678,12.1073709048319);
#731=CIRCLE('',#3680,12.8232171353527);
#732=CIRCLE('',#3682,12.1073709048319);
#733=CIRCLE('',#3685,2.37846096908266);
#734=CIRCLE('',#3686,0.2);
#735=CIRCLE('',#3687,2.17846096908266);
#736=CIRCLE('',#3689,5.15);
#737=CIRCLE('',#3691,2.17846096908266);
#738=CIRCLE('',#3693,2.4505);
#739=CIRCLE('',#3695,2.4505);
#740=CIRCLE('',#3698,12.8319377609308);
#741=CIRCLE('',#3699,4.96627380657387);
#742=CIRCLE('',#3700,4.96627380657387);
#811=ELLIPSE('',#3643,1.892,0.946);
#812=ELLIPSE('',#3645,1.892,0.946);
#813=ELLIPSE('',#3650,1.892,0.946);
#814=ELLIPSE('',#3655,1.892,0.946);
#815=ELLIPSE('',#3660,1.892,0.946);
#816=ELLIPSE('',#3664,1.892,0.946);
#817=ELLIPSE('',#3666,1.892,0.946);
#818=ELLIPSE('',#3671,1.892,0.946);
#875=LINE('',#5327,#1169);
#876=LINE('',#5334,#1170);
#877=LINE('',#5338,#1171);
#878=LINE('',#5343,#1172);
#879=LINE('',#5346,#1173);
#880=LINE('',#5350,#1174);
#881=LINE('',#5372,#1175);
#882=LINE('',#5376,#1176);
#883=LINE('',#5381,#1177);
#884=LINE('',#5384,#1178);
#885=LINE('',#5388,#1179);
#886=LINE('',#5408,#1180);
#887=LINE('',#5415,#1181);
#888=LINE('',#5419,#1182);
#889=LINE('',#5441,#1183);
#890=LINE('',#5445,#1184);
#891=LINE('',#5449,#1185);
#892=LINE('',#5453,#1186);
#893=LINE('',#5458,#1187);
#894=LINE('',#5461,#1188);
#895=LINE('',#5475,#1189);
#896=LINE('',#5479,#1190);
#897=LINE('',#5483,#1191);
#898=LINE('',#5492,#1192);
#1169=VECTOR('',#4190,10.);
#1170=VECTOR('',#4197,10.);
#1171=VECTOR('',#4202,10.);
#1172=VECTOR('',#4207,10.);
#1173=VECTOR('',#4210,10.);
#1174=VECTOR('',#4215,10.);
#1175=VECTOR('',#4222,10.);
#1176=VECTOR('',#4227,10.);
#1177=VECTOR('',#4232,10.);
#1178=VECTOR('',#4235,10.);
#1179=VECTOR('',#4240,10.);
#1180=VECTOR('',#4243,10.);
#1181=VECTOR('',#4250,10.);
#1182=VECTOR('',#4255,10.);
#1183=VECTOR('',#4262,10.);
#1184=VECTOR('',#4267,10.);
#1185=VECTOR('',#4272,10.);
#1186=VECTOR('',#4277,10.);
#1187=VECTOR('',#4284,10.);
#1188=VECTOR('',#4289,10.);
#1189=VECTOR('',#4308,2.17846096908266);
#1190=VECTOR('',#4313,2.33923048454133);
#1191=VECTOR('',#4318,2.5);
#1192=VECTOR('',#4331,5.05813690328693);
#1423=B_SPLINE_CURVE_WITH_KNOTS('',3,(#5311,#5312,#5313,#5314,#5315,#5316,
#5317,#5318,#5319,#5320,#5321,#5322,#5323,#5324,#5325),.UNSPECIFIED.,.F.,
 .F.,(4,2,2,3,2,2,4),(-0.0714521071173775,-0.0712222400952786,-0.0356111200476392,
0.,0.0356111200476392,0.0712222400952784,0.0714521071173274),
 .UNSPECIFIED.);
#1424=B_SPLINE_CURVE_WITH_KNOTS('',3,(#5353,#5354,#5355,#5356,#5357,#5358,
#5359,#5360,#5361,#5362,#5363,#5364,#5365,#5366,#5367),.UNSPECIFIED.,.F.,
 .F.,(4,2,2,3,2,2,4),(-0.071452107117379,-0.0712222400952786,-0.0356111200476392,
0.,0.0356111200476392,0.0712222400952784,0.071452107117329),
 .UNSPECIFIED.);
#1425=B_SPLINE_CURVE_WITH_KNOTS('',3,(#5392,#5393,#5394,#5395,#5396,#5397,
#5398,#5399,#5400,#5401,#5402,#5403,#5404,#5405,#5406),.UNSPECIFIED.,.F.,
 .F.,(4,2,2,3,2,2,4),(-0.0714521071173781,-0.0712222400952784,-0.0356111200476392,
0.,0.0356111200476392,0.0712222400952785,0.0714521071173282),
 .UNSPECIFIED.);
#1426=B_SPLINE_CURVE_WITH_KNOTS('',3,(#5422,#5423,#5424,#5425,#5426,#5427,
#5428,#5429,#5430,#5431,#5432,#5433,#5434,#5435,#5436),.UNSPECIFIED.,.F.,
 .F.,(4,2,2,3,2,2,4),(-0.0714521071173768,-0.0712222400952786,-0.0356111200476392,
0.,0.0356111200476392,0.0712222400952785,0.0714521071173268),
 .UNSPECIFIED.);
#1514=VERTEX_POINT('',#5309);
#1515=VERTEX_POINT('',#5310);
#1516=VERTEX_POINT('',#5326);
#1517=VERTEX_POINT('',#5328);
#1518=VERTEX_POINT('',#5330);
#1519=VERTEX_POINT('',#5332);
#1520=VERTEX_POINT('',#5336);
#1521=VERTEX_POINT('',#5340);
#1522=VERTEX_POINT('',#5342);
#1523=VERTEX_POINT('',#5344);
#1524=VERTEX_POINT('',#5348);
#1525=VERTEX_POINT('',#5352);
#1526=VERTEX_POINT('',#5368);
#1527=VERTEX_POINT('',#5370);
#1528=VERTEX_POINT('',#5374);
#1529=VERTEX_POINT('',#5378);
#1530=VERTEX_POINT('',#5380);
#1531=VERTEX_POINT('',#5382);
#1532=VERTEX_POINT('',#5386);
#1533=VERTEX_POINT('',#5390);
#1534=VERTEX_POINT('',#5391);
#1535=VERTEX_POINT('',#5407);
#1536=VERTEX_POINT('',#5409);
#1537=VERTEX_POINT('',#5411);
#1538=VERTEX_POINT('',#5413);
#1539=VERTEX_POINT('',#5417);
#1540=VERTEX_POINT('',#5421);
#1541=VERTEX_POINT('',#5437);
#1542=VERTEX_POINT('',#5439);
#1543=VERTEX_POINT('',#5443);
#1544=VERTEX_POINT('',#5447);
#1545=VERTEX_POINT('',#5451);
#1546=VERTEX_POINT('',#5456);
#1547=VERTEX_POINT('',#5464);
#1548=VERTEX_POINT('',#5466);
#1549=VERTEX_POINT('',#5470);
#1550=VERTEX_POINT('',#5473);
#1551=VERTEX_POINT('',#5477);
#1552=VERTEX_POINT('',#5481);
#1553=VERTEX_POINT('',#5486);
#1554=VERTEX_POINT('',#5488);
#1871=EDGE_CURVE('',#1514,#1515,#1423,.T.);
#1872=EDGE_CURVE('',#1516,#1514,#875,.T.);
#1873=EDGE_CURVE('',#1516,#1517,#811,.F.);
#1874=EDGE_CURVE('',#1517,#1518,#716,.F.);
#1875=EDGE_CURVE('',#1519,#1518,#812,.T.);
#1876=EDGE_CURVE('',#1515,#1519,#876,.T.);
#1877=EDGE_CURVE('',#1515,#1520,#717,.T.);
#1878=EDGE_CURVE('',#1520,#1519,#877,.F.);
#1879=EDGE_CURVE('',#1520,#1521,#718,.T.);
#1880=EDGE_CURVE('',#1518,#1522,#878,.F.);
#1881=EDGE_CURVE('',#1523,#1522,#813,.F.);
#1882=EDGE_CURVE('',#1521,#1523,#879,.T.);
#1883=EDGE_CURVE('',#1521,#1524,#719,.T.);
#1884=EDGE_CURVE('',#1523,#1524,#880,.T.);
#1885=EDGE_CURVE('',#1524,#1525,#1424,.T.);
#1886=EDGE_CURVE('',#1522,#1526,#720,.F.);
#1887=EDGE_CURVE('',#1527,#1526,#814,.T.);
#1888=EDGE_CURVE('',#1525,#1527,#881,.T.);
#1889=EDGE_CURVE('',#1525,#1528,#721,.T.);
#1890=EDGE_CURVE('',#1528,#1527,#882,.F.);
#1891=EDGE_CURVE('',#1528,#1529,#722,.T.);
#1892=EDGE_CURVE('',#1526,#1530,#883,.F.);
#1893=EDGE_CURVE('',#1531,#1530,#815,.F.);
#1894=EDGE_CURVE('',#1529,#1531,#884,.T.);
#1895=EDGE_CURVE('',#1529,#1532,#723,.T.);
#1896=EDGE_CURVE('',#1531,#1532,#885,.T.);
#1897=EDGE_CURVE('',#1533,#1534,#1425,.T.);
#1898=EDGE_CURVE('',#1535,#1533,#886,.T.);
#1899=EDGE_CURVE('',#1535,#1536,#816,.F.);
#1900=EDGE_CURVE('',#1536,#1537,#724,.F.);
#1901=EDGE_CURVE('',#1538,#1537,#817,.T.);
#1902=EDGE_CURVE('',#1534,#1538,#887,.T.);
#1903=EDGE_CURVE('',#1534,#1539,#725,.T.);
#1904=EDGE_CURVE('',#1539,#1538,#888,.F.);
#1905=EDGE_CURVE('',#1532,#1540,#1426,.T.);
#1906=EDGE_CURVE('',#1530,#1541,#726,.F.);
#1907=EDGE_CURVE('',#1542,#1541,#818,.T.);
#1908=EDGE_CURVE('',#1540,#1542,#889,.T.);
#1909=EDGE_CURVE('',#1540,#1543,#727,.T.);
#1910=EDGE_CURVE('',#1543,#1542,#890,.F.);
#1911=EDGE_CURVE('',#1544,#1514,#728,.T.);
#1912=EDGE_CURVE('',#1544,#1516,#891,.T.);
#1913=EDGE_CURVE('',#1539,#1545,#729,.T.);
#1914=EDGE_CURVE('',#1537,#1517,#892,.F.);
#1915=EDGE_CURVE('',#1545,#1544,#730,.T.);
#1916=EDGE_CURVE('',#1546,#1533,#731,.T.);
#1917=EDGE_CURVE('',#1546,#1535,#893,.T.);
#1918=EDGE_CURVE('',#1543,#1546,#732,.T.);
#1919=EDGE_CURVE('',#1541,#1536,#894,.F.);
#1920=EDGE_CURVE('',#1547,#1547,#733,.T.);
#1921=EDGE_CURVE('',#1547,#1548,#734,.T.);
#1922=EDGE_CURVE('',#1548,#1548,#735,.T.);
#1923=EDGE_CURVE('',#1549,#1549,#736,.T.);
#1924=EDGE_CURVE('',#1550,#1550,#737,.T.);
#1925=EDGE_CURVE('',#1550,#1548,#895,.T.);
#1926=EDGE_CURVE('',#1551,#1551,#738,.T.);
#1927=EDGE_CURVE('',#1551,#1550,#896,.T.);
#1928=EDGE_CURVE('',#1552,#1552,#739,.F.);
#1929=EDGE_CURVE('',#1552,#1551,#897,.T.);
#1930=EDGE_CURVE('',#1545,#1553,#740,.T.);
#1931=EDGE_CURVE('',#1554,#1553,#741,.T.);
#1932=EDGE_CURVE('',#1553,#1554,#742,.T.);
#1933=EDGE_CURVE('',#1549,#1554,#898,.T.);
#2473=ORIENTED_EDGE('',*,*,#1871,.F.);
#2474=ORIENTED_EDGE('',*,*,#1872,.F.);
#2475=ORIENTED_EDGE('',*,*,#1873,.T.);
#2476=ORIENTED_EDGE('',*,*,#1874,.T.);
#2477=ORIENTED_EDGE('',*,*,#1875,.F.);
#2478=ORIENTED_EDGE('',*,*,#1876,.F.);
#2479=ORIENTED_EDGE('',*,*,#1877,.F.);
#2480=ORIENTED_EDGE('',*,*,#1876,.T.);
#2481=ORIENTED_EDGE('',*,*,#1878,.F.);
#2482=ORIENTED_EDGE('',*,*,#1879,.F.);
#2483=ORIENTED_EDGE('',*,*,#1878,.T.);
#2484=ORIENTED_EDGE('',*,*,#1875,.T.);
#2485=ORIENTED_EDGE('',*,*,#1880,.T.);
#2486=ORIENTED_EDGE('',*,*,#1881,.F.);
#2487=ORIENTED_EDGE('',*,*,#1882,.F.);
#2488=ORIENTED_EDGE('',*,*,#1883,.F.);
#2489=ORIENTED_EDGE('',*,*,#1882,.T.);
#2490=ORIENTED_EDGE('',*,*,#1884,.T.);
#2491=ORIENTED_EDGE('',*,*,#1885,.F.);
#2492=ORIENTED_EDGE('',*,*,#1884,.F.);
#2493=ORIENTED_EDGE('',*,*,#1881,.T.);
#2494=ORIENTED_EDGE('',*,*,#1886,.T.);
#2495=ORIENTED_EDGE('',*,*,#1887,.F.);
#2496=ORIENTED_EDGE('',*,*,#1888,.F.);
#2497=ORIENTED_EDGE('',*,*,#1889,.F.);
#2498=ORIENTED_EDGE('',*,*,#1888,.T.);
#2499=ORIENTED_EDGE('',*,*,#1890,.F.);
#2500=ORIENTED_EDGE('',*,*,#1891,.F.);
#2501=ORIENTED_EDGE('',*,*,#1890,.T.);
#2502=ORIENTED_EDGE('',*,*,#1887,.T.);
#2503=ORIENTED_EDGE('',*,*,#1892,.T.);
#2504=ORIENTED_EDGE('',*,*,#1893,.F.);
#2505=ORIENTED_EDGE('',*,*,#1894,.F.);
#2506=ORIENTED_EDGE('',*,*,#1895,.F.);
#2507=ORIENTED_EDGE('',*,*,#1894,.T.);
#2508=ORIENTED_EDGE('',*,*,#1896,.T.);
#2509=ORIENTED_EDGE('',*,*,#1897,.F.);
#2510=ORIENTED_EDGE('',*,*,#1898,.F.);
#2511=ORIENTED_EDGE('',*,*,#1899,.T.);
#2512=ORIENTED_EDGE('',*,*,#1900,.T.);
#2513=ORIENTED_EDGE('',*,*,#1901,.F.);
#2514=ORIENTED_EDGE('',*,*,#1902,.F.);
#2515=ORIENTED_EDGE('',*,*,#1903,.F.);
#2516=ORIENTED_EDGE('',*,*,#1902,.T.);
#2517=ORIENTED_EDGE('',*,*,#1904,.F.);
#2518=ORIENTED_EDGE('',*,*,#1905,.F.);
#2519=ORIENTED_EDGE('',*,*,#1896,.F.);
#2520=ORIENTED_EDGE('',*,*,#1893,.T.);
#2521=ORIENTED_EDGE('',*,*,#1906,.T.);
#2522=ORIENTED_EDGE('',*,*,#1907,.F.);
#2523=ORIENTED_EDGE('',*,*,#1908,.F.);
#2524=ORIENTED_EDGE('',*,*,#1909,.F.);
#2525=ORIENTED_EDGE('',*,*,#1908,.T.);
#2526=ORIENTED_EDGE('',*,*,#1910,.F.);
#2527=ORIENTED_EDGE('',*,*,#1911,.F.);
#2528=ORIENTED_EDGE('',*,*,#1912,.T.);
#2529=ORIENTED_EDGE('',*,*,#1872,.T.);
#2530=ORIENTED_EDGE('',*,*,#1913,.F.);
#2531=ORIENTED_EDGE('',*,*,#1904,.T.);
#2532=ORIENTED_EDGE('',*,*,#1901,.T.);
#2533=ORIENTED_EDGE('',*,*,#1914,.T.);
#2534=ORIENTED_EDGE('',*,*,#1873,.F.);
#2535=ORIENTED_EDGE('',*,*,#1912,.F.);
#2536=ORIENTED_EDGE('',*,*,#1915,.F.);
#2537=ORIENTED_EDGE('',*,*,#1916,.F.);
#2538=ORIENTED_EDGE('',*,*,#1917,.T.);
#2539=ORIENTED_EDGE('',*,*,#1898,.T.);
#2540=ORIENTED_EDGE('',*,*,#1918,.F.);
#2541=ORIENTED_EDGE('',*,*,#1910,.T.);
#2542=ORIENTED_EDGE('',*,*,#1907,.T.);
#2543=ORIENTED_EDGE('',*,*,#1919,.T.);
#2544=ORIENTED_EDGE('',*,*,#1899,.F.);
#2545=ORIENTED_EDGE('',*,*,#1917,.F.);
#2546=ORIENTED_EDGE('',*,*,#1880,.F.);
#2547=ORIENTED_EDGE('',*,*,#1874,.F.);
#2548=ORIENTED_EDGE('',*,*,#1914,.F.);
#2549=ORIENTED_EDGE('',*,*,#1900,.F.);
#2550=ORIENTED_EDGE('',*,*,#1919,.F.);
#2551=ORIENTED_EDGE('',*,*,#1906,.F.);
#2552=ORIENTED_EDGE('',*,*,#1892,.F.);
#2553=ORIENTED_EDGE('',*,*,#1886,.F.);
#2554=ORIENTED_EDGE('',*,*,#1920,.T.);
#2555=ORIENTED_EDGE('',*,*,#1921,.T.);
#2556=ORIENTED_EDGE('',*,*,#1922,.T.);
#2557=ORIENTED_EDGE('',*,*,#1921,.F.);
#2558=ORIENTED_EDGE('',*,*,#1923,.T.);
#2559=ORIENTED_EDGE('',*,*,#1920,.F.);
#2560=ORIENTED_EDGE('',*,*,#1924,.F.);
#2561=ORIENTED_EDGE('',*,*,#1925,.T.);
#2562=ORIENTED_EDGE('',*,*,#1922,.F.);
#2563=ORIENTED_EDGE('',*,*,#1925,.F.);
#2564=ORIENTED_EDGE('',*,*,#1926,.F.);
#2565=ORIENTED_EDGE('',*,*,#1927,.T.);
#2566=ORIENTED_EDGE('',*,*,#1924,.T.);
#2567=ORIENTED_EDGE('',*,*,#1927,.F.);
#2568=ORIENTED_EDGE('',*,*,#1928,.F.);
#2569=ORIENTED_EDGE('',*,*,#1929,.T.);
#2570=ORIENTED_EDGE('',*,*,#1926,.T.);
#2571=ORIENTED_EDGE('',*,*,#1929,.F.);
#2572=ORIENTED_EDGE('',*,*,#1928,.T.);
#2573=ORIENTED_EDGE('',*,*,#1905,.T.);
#2574=ORIENTED_EDGE('',*,*,#1909,.T.);
#2575=ORIENTED_EDGE('',*,*,#1918,.T.);
#2576=ORIENTED_EDGE('',*,*,#1916,.T.);
#2577=ORIENTED_EDGE('',*,*,#1897,.T.);
#2578=ORIENTED_EDGE('',*,*,#1903,.T.);
#2579=ORIENTED_EDGE('',*,*,#1913,.T.);
#2580=ORIENTED_EDGE('',*,*,#1930,.T.);
#2581=ORIENTED_EDGE('',*,*,#1931,.F.);
#2582=ORIENTED_EDGE('',*,*,#1932,.F.);
#2583=ORIENTED_EDGE('',*,*,#1930,.F.);
#2584=ORIENTED_EDGE('',*,*,#1915,.T.);
#2585=ORIENTED_EDGE('',*,*,#1911,.T.);
#2586=ORIENTED_EDGE('',*,*,#1871,.T.);
#2587=ORIENTED_EDGE('',*,*,#1877,.T.);
#2588=ORIENTED_EDGE('',*,*,#1879,.T.);
#2589=ORIENTED_EDGE('',*,*,#1883,.T.);
#2590=ORIENTED_EDGE('',*,*,#1885,.T.);
#2591=ORIENTED_EDGE('',*,*,#1889,.T.);
#2592=ORIENTED_EDGE('',*,*,#1891,.T.);
#2593=ORIENTED_EDGE('',*,*,#1895,.T.);
#2594=ORIENTED_EDGE('',*,*,#1923,.F.);
#2595=ORIENTED_EDGE('',*,*,#1933,.T.);
#2596=ORIENTED_EDGE('',*,*,#1931,.T.);
#2597=ORIENTED_EDGE('',*,*,#1932,.T.);
#2598=ORIENTED_EDGE('',*,*,#1933,.F.);
#3185=CYLINDRICAL_SURFACE('',#3642,0.946);
#3186=CYLINDRICAL_SURFACE('',#3653,0.946);
#3187=CYLINDRICAL_SURFACE('',#3663,0.946);
#3188=CYLINDRICAL_SURFACE('',#3669,0.946);
#3189=CYLINDRICAL_SURFACE('',#3690,2.17846096908266);
#3190=CYLINDRICAL_SURFACE('',#3694,2.4505);
#3258=ADVANCED_FACE('',(#316),#3185,.T.);
#3259=ADVANCED_FACE('',(#317),#159,.F.);
#3260=ADVANCED_FACE('',(#318),#160,.F.);
#3261=ADVANCED_FACE('',(#319),#161,.F.);
#3262=ADVANCED_FACE('',(#320),#3186,.T.);
#3263=ADVANCED_FACE('',(#321),#162,.F.);
#3264=ADVANCED_FACE('',(#322),#163,.F.);
#3265=ADVANCED_FACE('',(#323),#164,.F.);
#3266=ADVANCED_FACE('',(#324),#3187,.T.);
#3267=ADVANCED_FACE('',(#325),#165,.F.);
#3268=ADVANCED_FACE('',(#326),#3188,.T.);
#3269=ADVANCED_FACE('',(#327),#166,.F.);
#3270=ADVANCED_FACE('',(#328),#167,.F.);
#3271=ADVANCED_FACE('',(#329),#168,.F.);
#3272=ADVANCED_FACE('',(#330),#169,.F.);
#3273=ADVANCED_FACE('',(#331),#170,.F.);
#3274=ADVANCED_FACE('',(#332),#171,.F.);
#3275=ADVANCED_FACE('',(#333),#127,.F.);
#3276=ADVANCED_FACE('',(#334,#109),#172,.T.);
#3277=ADVANCED_FACE('',(#335),#3189,.T.);
#3278=ADVANCED_FACE('',(#336),#103,.T.);
#3279=ADVANCED_FACE('',(#337),#3190,.T.);
#3280=ADVANCED_FACE('',(#338),#173,.T.);
#3281=ADVANCED_FACE('',(#339),#97,.T.);
#3282=ADVANCED_FACE('',(#340),#104,.T.);
#3399=CLOSED_SHELL('',(#3258,#3259,#3260,#3261,#3262,#3263,#3264,#3265,
#3266,#3267,#3268,#3269,#3270,#3271,#3272,#3273,#3274,#3275,#3276,#3277,
#3278,#3279,#3280,#3281,#3282));
#3641=AXIS2_PLACEMENT_3D('',#5307,#4186,#4187);
#3642=AXIS2_PLACEMENT_3D('',#5308,#4188,#4189);
#3643=AXIS2_PLACEMENT_3D('',#5329,#4191,#4192);
#3644=AXIS2_PLACEMENT_3D('',#5331,#4193,#4194);
#3645=AXIS2_PLACEMENT_3D('',#5333,#4195,#4196);
#3646=AXIS2_PLACEMENT_3D('',#5335,#4198,#4199);
#3647=AXIS2_PLACEMENT_3D('',#5337,#4200,#4201);
#3648=AXIS2_PLACEMENT_3D('',#5339,#4203,#4204);
#3649=AXIS2_PLACEMENT_3D('',#5341,#4205,#4206);
#3650=AXIS2_PLACEMENT_3D('',#5345,#4208,#4209);
#3651=AXIS2_PLACEMENT_3D('',#5347,#4211,#4212);
#3652=AXIS2_PLACEMENT_3D('',#5349,#4213,#4214);
#3653=AXIS2_PLACEMENT_3D('',#5351,#4216,#4217);
#3654=AXIS2_PLACEMENT_3D('',#5369,#4218,#4219);
#3655=AXIS2_PLACEMENT_3D('',#5371,#4220,#4221);
#3656=AXIS2_PLACEMENT_3D('',#5373,#4223,#4224);
#3657=AXIS2_PLACEMENT_3D('',#5375,#4225,#4226);
#3658=AXIS2_PLACEMENT_3D('',#5377,#4228,#4229);
#3659=AXIS2_PLACEMENT_3D('',#5379,#4230,#4231);
#3660=AXIS2_PLACEMENT_3D('',#5383,#4233,#4234);
#3661=AXIS2_PLACEMENT_3D('',#5385,#4236,#4237);
#3662=AXIS2_PLACEMENT_3D('',#5387,#4238,#4239);
#3663=AXIS2_PLACEMENT_3D('',#5389,#4241,#4242);
#3664=AXIS2_PLACEMENT_3D('',#5410,#4244,#4245);
#3665=AXIS2_PLACEMENT_3D('',#5412,#4246,#4247);
#3666=AXIS2_PLACEMENT_3D('',#5414,#4248,#4249);
#3667=AXIS2_PLACEMENT_3D('',#5416,#4251,#4252);
#3668=AXIS2_PLACEMENT_3D('',#5418,#4253,#4254);
#3669=AXIS2_PLACEMENT_3D('',#5420,#4256,#4257);
#3670=AXIS2_PLACEMENT_3D('',#5438,#4258,#4259);
#3671=AXIS2_PLACEMENT_3D('',#5440,#4260,#4261);
#3672=AXIS2_PLACEMENT_3D('',#5442,#4263,#4264);
#3673=AXIS2_PLACEMENT_3D('',#5444,#4265,#4266);
#3674=AXIS2_PLACEMENT_3D('',#5446,#4268,#4269);
#3675=AXIS2_PLACEMENT_3D('',#5448,#4270,#4271);
#3676=AXIS2_PLACEMENT_3D('',#5450,#4273,#4274);
#3677=AXIS2_PLACEMENT_3D('',#5452,#4275,#4276);
#3678=AXIS2_PLACEMENT_3D('',#5454,#4278,#4279);
#3679=AXIS2_PLACEMENT_3D('',#5455,#4280,#4281);
#3680=AXIS2_PLACEMENT_3D('',#5457,#4282,#4283);
#3681=AXIS2_PLACEMENT_3D('',#5459,#4285,#4286);
#3682=AXIS2_PLACEMENT_3D('',#5460,#4287,#4288);
#3683=AXIS2_PLACEMENT_3D('',#5462,#4290,#4291);
#3684=AXIS2_PLACEMENT_3D('',#5463,#4292,#4293);
#3685=AXIS2_PLACEMENT_3D('',#5465,#4294,#4295);
#3686=AXIS2_PLACEMENT_3D('',#5467,#4296,#4297);
#3687=AXIS2_PLACEMENT_3D('',#5468,#4298,#4299);
#3688=AXIS2_PLACEMENT_3D('',#5469,#4300,#4301);
#3689=AXIS2_PLACEMENT_3D('',#5471,#4302,#4303);
#3690=AXIS2_PLACEMENT_3D('',#5472,#4304,#4305);
#3691=AXIS2_PLACEMENT_3D('',#5474,#4306,#4307);
#3692=AXIS2_PLACEMENT_3D('',#5476,#4309,#4310);
#3693=AXIS2_PLACEMENT_3D('',#5478,#4311,#4312);
#3694=AXIS2_PLACEMENT_3D('',#5480,#4314,#4315);
#3695=AXIS2_PLACEMENT_3D('',#5482,#4316,#4317);
#3696=AXIS2_PLACEMENT_3D('',#5484,#4319,#4320);
#3697=AXIS2_PLACEMENT_3D('',#5485,#4321,#4322);
#3698=AXIS2_PLACEMENT_3D('',#5487,#4323,#4324);
#3699=AXIS2_PLACEMENT_3D('',#5489,#4325,#4326);
#3700=AXIS2_PLACEMENT_3D('',#5490,#4327,#4328);
#3701=AXIS2_PLACEMENT_3D('',#5491,#4329,#4330);
#4186=DIRECTION('axis',(0.,0.,1.));
#4187=DIRECTION('refdir',(1.,0.,0.));
#4188=DIRECTION('center_axis',(0.,0.,-1.));
#4189=DIRECTION('ref_axis',(0.707106781186563,-0.707106781186532,0.));
#4190=DIRECTION('',(0.,0.,1.));
#4191=DIRECTION('center_axis',(-0.866025403784439,0.,-0.5));
#4192=DIRECTION('ref_axis',(0.5,0.,-0.866025403784439));
#4193=DIRECTION('center_axis',(0.,0.,-1.));
#4194=DIRECTION('ref_axis',(0.707106781186563,-0.707106781186532,0.));
#4195=DIRECTION('center_axis',(-2.54091264057109E-15,0.866025403784439,
-0.5));
#4196=DIRECTION('ref_axis',(1.43032168209504E-15,-0.5,-0.866025403784439));
#4197=DIRECTION('',(0.,0.,-1.));
#4198=DIRECTION('center_axis',(-1.,-4.30300426108057E-14,0.));
#4199=DIRECTION('ref_axis',(-4.30300426108057E-14,1.,0.));
#4200=DIRECTION('center_axis',(-1.,-4.30300426108057E-14,0.));
#4201=DIRECTION('ref_axis',(0.,0.,-1.));
#4202=DIRECTION('',(-2.15150213054029E-14,0.5,0.866025403784439));
#4203=DIRECTION('center_axis',(-2.54091264057109E-15,0.866025403784439,
-0.5));
#4204=DIRECTION('ref_axis',(1.,2.93399319404209E-15,0.));
#4205=DIRECTION('center_axis',(-2.54091264057109E-15,0.866025403784439,
-0.5));
#4206=DIRECTION('ref_axis',(0.,-0.5,-0.866025403784439));
#4207=DIRECTION('',(-1.,-2.93399319404209E-15,0.));
#4208=DIRECTION('center_axis',(-2.54091264057109E-15,0.866025403784439,
-0.5));
#4209=DIRECTION('ref_axis',(1.46699659702056E-15,-0.5,-0.866025403784439));
#4210=DIRECTION('',(-1.73044443434865E-14,-0.5,-0.866025403784439));
#4211=DIRECTION('center_axis',(1.,-3.4608888686973E-14,0.));
#4212=DIRECTION('ref_axis',(-3.4608888686973E-14,-1.,0.));
#4213=DIRECTION('center_axis',(1.,-3.4608888686973E-14,0.));
#4214=DIRECTION('ref_axis',(0.,0.,1.));
#4215=DIRECTION('',(0.,0.,1.));
#4216=DIRECTION('center_axis',(0.,0.,-1.));
#4217=DIRECTION('ref_axis',(-0.707106781186546,-0.707106781186549,0.));
#4218=DIRECTION('center_axis',(0.,0.,-1.));
#4219=DIRECTION('ref_axis',(-0.707106781186546,-0.707106781186549,0.));
#4220=DIRECTION('center_axis',(0.866025403784439,0.,-0.5));
#4221=DIRECTION('ref_axis',(-0.5,-3.66749149255139E-17,-0.866025403784439));
#4222=DIRECTION('',(0.,0.,-1.));
#4223=DIRECTION('center_axis',(-4.04626176340286E-14,1.,0.));
#4224=DIRECTION('ref_axis',(1.,4.04626176340286E-14,0.));
#4225=DIRECTION('center_axis',(-4.04626176340286E-14,1.,0.));
#4226=DIRECTION('ref_axis',(0.,0.,-1.));
#4227=DIRECTION('',(0.5,2.02313088170143E-14,0.866025403784439));
#4228=DIRECTION('center_axis',(0.866025403784439,0.,-0.5));
#4229=DIRECTION('ref_axis',(0.,-1.,0.));
#4230=DIRECTION('center_axis',(0.866025403784439,0.,-0.5));
#4231=DIRECTION('ref_axis',(0.5,0.,0.866025403784439));
#4232=DIRECTION('',(0.,1.,0.));
#4233=DIRECTION('center_axis',(0.866025403784439,0.,-0.5));
#4234=DIRECTION('ref_axis',(-0.5,3.66749149255139E-17,-0.866025403784439));
#4235=DIRECTION('',(-0.5,2.39626331165986E-16,-0.866025403784439));
#4236=DIRECTION('center_axis',(-4.79252662331972E-16,-1.,0.));
#4237=DIRECTION('ref_axis',(-1.,4.79252662331972E-16,0.));
#4238=DIRECTION('center_axis',(-4.79252662331972E-16,-1.,0.));
#4239=DIRECTION('ref_axis',(0.,0.,1.));
#4240=DIRECTION('',(0.,0.,1.));
#4241=DIRECTION('center_axis',(0.,0.,-1.));
#4242=DIRECTION('ref_axis',(0.70710678118653,0.707106781186565,0.));
#4243=DIRECTION('',(0.,0.,1.));
#4244=DIRECTION('center_axis',(-1.27045632028555E-15,-0.866025403784439,
-0.5));
#4245=DIRECTION('ref_axis',(6.96823383584764E-16,0.5,-0.866025403784439));
#4246=DIRECTION('center_axis',(0.,0.,-1.));
#4247=DIRECTION('ref_axis',(0.70710678118653,0.707106781186565,0.));
#4248=DIRECTION('center_axis',(-0.866025403784439,0.,-0.5));
#4249=DIRECTION('ref_axis',(0.5,3.66749149255139E-17,-0.866025403784439));
#4250=DIRECTION('',(0.,0.,-1.));
#4251=DIRECTION('center_axis',(5.35736011821097E-14,-1.,0.));
#4252=DIRECTION('ref_axis',(-1.,-5.35736011821097E-14,0.));
#4253=DIRECTION('center_axis',(5.35736011821097E-14,-1.,0.));
#4254=DIRECTION('ref_axis',(0.,0.,1.));
#4255=DIRECTION('',(-0.5,-2.67868005910549E-14,0.866025403784439));
#4256=DIRECTION('center_axis',(0.,0.,-1.));
#4257=DIRECTION('ref_axis',(-0.707106781186557,0.707106781186538,0.));
#4258=DIRECTION('center_axis',(0.,0.,-1.));
#4259=DIRECTION('ref_axis',(-0.707106781186557,0.707106781186538,0.));
#4260=DIRECTION('center_axis',(-1.27045632028555E-15,-0.866025403784439,
-0.5));
#4261=DIRECTION('ref_axis',(7.33498298510278E-16,0.5,-0.866025403784439));
#4262=DIRECTION('',(0.,0.,-1.));
#4263=DIRECTION('center_axis',(1.,2.81047454124667E-14,0.));
#4264=DIRECTION('ref_axis',(2.81047454124667E-14,-1.,0.));
#4265=DIRECTION('center_axis',(1.,2.81047454124667E-14,0.));
#4266=DIRECTION('ref_axis',(0.,0.,1.));
#4267=DIRECTION('',(1.40523727062334E-14,-0.5,0.866025403784439));
#4268=DIRECTION('center_axis',(0.,1.,0.));
#4269=DIRECTION('ref_axis',(1.,0.,0.));
#4270=DIRECTION('center_axis',(0.,1.,0.));
#4271=DIRECTION('ref_axis',(0.,0.,-1.));
#4272=DIRECTION('',(0.5,0.,-0.866025403784439));
#4273=DIRECTION('center_axis',(-0.866025403784439,0.,-0.5));
#4274=DIRECTION('ref_axis',(0.,1.,0.));
#4275=DIRECTION('center_axis',(-0.866025403784439,0.,-0.5));
#4276=DIRECTION('ref_axis',(0.5,0.,-0.866025403784439));
#4277=DIRECTION('',(0.,-1.,0.));
#4278=DIRECTION('center_axis',(-0.866025403784439,0.,-0.5));
#4279=DIRECTION('ref_axis',(0.5,0.,-0.866025403784439));
#4280=DIRECTION('center_axis',(-1.,3.8682536316795E-15,0.));
#4281=DIRECTION('ref_axis',(3.8682536316795E-15,1.,0.));
#4282=DIRECTION('center_axis',(-1.,3.8682536316795E-15,0.));
#4283=DIRECTION('ref_axis',(0.,0.,-1.));
#4284=DIRECTION('',(1.93412681583975E-15,0.5,-0.866025403784439));
#4285=DIRECTION('center_axis',(-1.27045632028555E-15,-0.866025403784439,
-0.5));
#4286=DIRECTION('ref_axis',(-1.,1.46699659702105E-15,0.));
#4287=DIRECTION('center_axis',(-1.27045632028555E-15,-0.866025403784439,
-0.5));
#4288=DIRECTION('ref_axis',(0.,-0.5,0.866025403784439));
#4289=DIRECTION('',(1.,-1.46699659702105E-15,0.));
#4290=DIRECTION('center_axis',(0.,0.,-1.));
#4291=DIRECTION('ref_axis',(-1.,0.,0.));
#4292=DIRECTION('center_axis',(0.,0.,-1.));
#4293=DIRECTION('ref_axis',(-1.,0.,0.));
#4294=DIRECTION('center_axis',(0.,0.,-1.));
#4295=DIRECTION('ref_axis',(1.,0.,0.));
#4296=DIRECTION('center_axis',(-1.22464679914735E-16,-1.,0.));
#4297=DIRECTION('ref_axis',(1.,-1.22464679914735E-16,0.));
#4298=DIRECTION('center_axis',(0.,0.,1.));
#4299=DIRECTION('ref_axis',(1.,0.,0.));
#4300=DIRECTION('center_axis',(0.,0.,-1.));
#4301=DIRECTION('ref_axis',(-1.,0.,0.));
#4302=DIRECTION('center_axis',(0.,0.,-1.));
#4303=DIRECTION('ref_axis',(1.,0.,0.));
#4304=DIRECTION('center_axis',(0.,0.,-1.));
#4305=DIRECTION('ref_axis',(-1.,0.,0.));
#4306=DIRECTION('center_axis',(0.,0.,-1.));
#4307=DIRECTION('ref_axis',(1.,0.,0.));
#4308=DIRECTION('',(0.,0.,1.));
#4309=DIRECTION('center_axis',(0.,0.,-1.));
#4310=DIRECTION('ref_axis',(-1.,0.,0.));
#4311=DIRECTION('center_axis',(0.,0.,-1.));
#4312=DIRECTION('ref_axis',(-1.,0.,0.));
#4313=DIRECTION('',(-0.258819045102519,3.16961915143174E-17,0.965925826289069));
#4314=DIRECTION('center_axis',(0.,0.,-1.));
#4315=DIRECTION('ref_axis',(-1.,0.,0.));
#4316=DIRECTION('center_axis',(0.,0.,1.));
#4317=DIRECTION('ref_axis',(-1.,0.,0.));
#4318=DIRECTION('',(0.,0.,1.));
#4319=DIRECTION('center_axis',(0.,0.,-1.));
#4320=DIRECTION('ref_axis',(-1.,0.,0.));
#4321=DIRECTION('center_axis',(6.12323399573676E-17,0.,1.));
#4322=DIRECTION('ref_axis',(1.,0.,0.));
#4323=DIRECTION('center_axis',(1.22464679914735E-16,-1.,0.));
#4324=DIRECTION('ref_axis',(-1.,-1.22464679914735E-16,0.));
#4325=DIRECTION('center_axis',(0.,0.,-1.));
#4326=DIRECTION('ref_axis',(1.,0.,0.));
#4327=DIRECTION('center_axis',(0.,0.,-1.));
#4328=DIRECTION('ref_axis',(1.,0.,0.));
#4329=DIRECTION('center_axis',(0.,0.,-1.));
#4330=DIRECTION('ref_axis',(-1.,0.,0.));
#4331=DIRECTION('',(-0.0871557427578718,1.06735001395738E-17,0.996194698090852));
#5307=CARTESIAN_POINT('',(0.,0.,0.));
#5308=CARTESIAN_POINT('Origin',(-1.41899999999985,1.41899999999965,3.1));
#5309=CARTESIAN_POINT('',(-1.41899999999985,0.472999999999654,3.01252522110193));
#5310=CARTESIAN_POINT('',(-0.472999999999848,1.41899999999969,3.01252522110194));
#5311=CARTESIAN_POINT('Ctrl Pts',(-1.41899999999985,0.472999999999654,3.01252522110193));
#5312=CARTESIAN_POINT('Ctrl Pts',(-1.418237843063,0.472999999999654,3.01261008153857));
#5313=CARTESIAN_POINT('Ctrl Pts',(-1.41747599318127,0.473000921064105,3.01269480438576));
#5314=CARTESIAN_POINT('Ctrl Pts',(-1.29873656917598,0.473287797471327,3.02588334070707));
#5315=CARTESIAN_POINT('Ctrl Pts',(-1.17260477262757,0.497030428020145,3.03726209636997));
#5316=CARTESIAN_POINT('Ctrl Pts',(-0.940241249793281,0.593452559529333,
3.05235989856665));
#5317=CARTESIAN_POINT('Ctrl Pts',(-0.834013199901804,0.666140770092746,
3.05607990145755));
#5318=CARTESIAN_POINT('Ctrl Pts',(-0.75007698499736,0.750076984997194,3.05607990145756));
#5319=CARTESIAN_POINT('Ctrl Pts',(-0.666140770092915,0.834013199901643,
3.05607990145756));
#5320=CARTESIAN_POINT('Ctrl Pts',(-0.593452559529506,0.940241249793123,
3.05235989856665));
#5321=CARTESIAN_POINT('Ctrl Pts',(-0.497030428020328,1.17260477262741,3.03726209636997));
#5322=CARTESIAN_POINT('Ctrl Pts',(-0.473287797471517,1.29873656917583,3.02588334070708));
#5323=CARTESIAN_POINT('Ctrl Pts',(-0.4730009210643,1.41747599318095,3.01269480438579));
#5324=CARTESIAN_POINT('Ctrl Pts',(-0.472999999999848,1.41823784306269,3.0126100815386));
#5325=CARTESIAN_POINT('Ctrl Pts',(-0.472999999999848,1.41899999999969,3.01252522110194));
#5326=CARTESIAN_POINT('',(-1.41899999999985,0.472999999999654,1.22765307701778));
#5327=CARTESIAN_POINT('',(-1.41899999999985,0.472999999999654,3.1));
#5328=CARTESIAN_POINT('',(-0.866098738193358,0.651395808574938,0.27));
#5329=CARTESIAN_POINT('Origin',(-1.41899999999985,1.41899999999965,1.22765307701778));
#5330=CARTESIAN_POINT('',(-0.651395808574991,0.86609873819336,0.27));
#5331=CARTESIAN_POINT('Origin',(-1.41899999999985,1.41899999999965,0.27));
#5332=CARTESIAN_POINT('',(-0.472999999999848,1.41899999999969,1.22765307701751));
#5333=CARTESIAN_POINT('Origin',(-1.41899999999985,1.41899999999965,1.22765307701745));
#5334=CARTESIAN_POINT('',(-0.472999999999848,1.41899999999969,3.1));
#5335=CARTESIAN_POINT('Origin',(-0.472999999999807,0.472999999999754,3.1));
#5336=CARTESIAN_POINT('',(-0.472999999999889,2.36767196216383,2.87080111520185));
#5337=CARTESIAN_POINT('Origin',(-0.472999999999787,-2.0353210154902E-14,
-9.73193776093083));
#5338=CARTESIAN_POINT('',(-0.472999999999884,2.24662499999997,2.66114162663218));
#5339=CARTESIAN_POINT('Origin',(-0.472999999999895,2.5,3.1));
#5340=CARTESIAN_POINT('',(0.472999999999787,2.36767196216383,2.87080111520185));
#5341=CARTESIAN_POINT('Origin',(1.16338464595253E-14,-3.68139204037345,
-7.60648507542867));
#5342=CARTESIAN_POINT('',(0.651395808575038,0.866098738193364,0.27));
#5343=CARTESIAN_POINT('',(-0.236499999999946,0.866098738193362,0.27));
#5344=CARTESIAN_POINT('',(0.472999999999754,1.41899999999989,1.22765307701784));
#5345=CARTESIAN_POINT('Origin',(1.41899999999975,1.41899999999985,1.22765307701778));
#5346=CARTESIAN_POINT('',(0.472999999999791,2.5,3.09999999999999));
#5347=CARTESIAN_POINT('Origin',(0.472999999999791,2.5,3.1));
#5348=CARTESIAN_POINT('',(0.472999999999754,1.41899999999989,3.01252522110192));
#5349=CARTESIAN_POINT('Origin',(0.472999999999705,-1.6370004348928E-14,
-9.73193776093083));
#5350=CARTESIAN_POINT('',(0.472999999999754,1.41899999999989,3.1));
#5351=CARTESIAN_POINT('Origin',(1.41899999999975,1.41899999999985,3.1));
#5352=CARTESIAN_POINT('',(1.41899999999979,0.472999999999854,3.01252522110193));
#5353=CARTESIAN_POINT('Ctrl Pts',(0.472999999999754,1.41899999999989,3.01252522110192));
#5354=CARTESIAN_POINT('Ctrl Pts',(0.472999999999754,1.41823784306304,3.01261008153856));
#5355=CARTESIAN_POINT('Ctrl Pts',(0.473000921064206,1.4174759931813,3.01269480438575));
#5356=CARTESIAN_POINT('Ctrl Pts',(0.473287797471426,1.29873656917601,3.02588334070706));
#5357=CARTESIAN_POINT('Ctrl Pts',(0.49703042802024,1.17260477262759,3.03726209636996));
#5358=CARTESIAN_POINT('Ctrl Pts',(0.593452559529424,0.940241249793303,3.05235989856665));
#5359=CARTESIAN_POINT('Ctrl Pts',(0.666140770092836,0.834013199901824,3.05607990145755));
#5360=CARTESIAN_POINT('Ctrl Pts',(0.750076984997282,0.750076984997378,3.05607990145755));
#5361=CARTESIAN_POINT('Ctrl Pts',(0.834013199901729,0.666140770092932,3.05607990145755));
#5362=CARTESIAN_POINT('Ctrl Pts',(0.940241249793208,0.593452559529521,3.05235989856665));
#5363=CARTESIAN_POINT('Ctrl Pts',(1.1726047726275,0.497030428020338,3.03726209636996));
#5364=CARTESIAN_POINT('Ctrl Pts',(1.29873656917591,0.473287797471525,3.02588334070707));
#5365=CARTESIAN_POINT('Ctrl Pts',(1.41747599318104,0.473000921064306,3.01269480438578));
#5366=CARTESIAN_POINT('Ctrl Pts',(1.41823784306278,0.472999999999854,3.01261008153858));
#5367=CARTESIAN_POINT('Ctrl Pts',(1.41899999999979,0.472999999999854,3.01252522110193));
#5368=CARTESIAN_POINT('',(0.866098738193361,0.651395808575069,0.27));
#5369=CARTESIAN_POINT('Origin',(1.41899999999975,1.41899999999985,0.27));
#5370=CARTESIAN_POINT('',(1.41899999999979,0.472999999999853,1.22765307701768));
#5371=CARTESIAN_POINT('Origin',(1.41899999999975,1.41899999999985,1.22765307701762));
#5372=CARTESIAN_POINT('',(1.41899999999979,0.472999999999854,3.1));
#5373=CARTESIAN_POINT('Origin',(0.472999999999817,0.472999999999815,3.1));
#5374=CARTESIAN_POINT('',(2.36767196216383,0.472999999999892,2.87080111520185));
#5375=CARTESIAN_POINT('Origin',(-1.83061508724184E-14,0.472999999999796,
-9.73193776093083));
#5376=CARTESIAN_POINT('',(2.24662499999998,0.472999999999887,2.6611416266322));
#5377=CARTESIAN_POINT('Origin',(2.5,0.472999999999897,3.1));
#5378=CARTESIAN_POINT('',(2.36767196216383,-0.472999999999786,2.87080111520185));
#5379=CARTESIAN_POINT('Origin',(-3.68139204037345,0.,-7.60648507542867));
#5380=CARTESIAN_POINT('',(0.866098738193361,-0.65139580857508,0.270000000000001));
#5381=CARTESIAN_POINT('',(0.86609873819336,0.236499999999951,0.27));
#5382=CARTESIAN_POINT('',(1.41899999999987,-0.472999999999785,1.22765307701781));
#5383=CARTESIAN_POINT('Origin',(1.41899999999987,-1.41899999999979,1.22765307701781));
#5384=CARTESIAN_POINT('',(2.5,-0.472999999999786,3.1));
#5385=CARTESIAN_POINT('Origin',(2.5,-0.472999999999786,3.1));
#5386=CARTESIAN_POINT('',(1.41899999999987,-0.472999999999785,3.01252522110192));
#5387=CARTESIAN_POINT('Origin',(6.05980759185948E-16,-0.472999999999784,
-9.73193776093083));
#5388=CARTESIAN_POINT('',(1.41899999999987,-0.472999999999785,3.1));
#5389=CARTESIAN_POINT('Origin',(-1.41899999999978,-1.41899999999983,3.1));
#5390=CARTESIAN_POINT('',(-0.472999999999784,-1.41899999999984,3.01252522110192));
#5391=CARTESIAN_POINT('',(-1.41899999999983,-0.472999999999835,3.01252522110192));
#5392=CARTESIAN_POINT('Ctrl Pts',(-0.472999999999784,-1.41899999999984,
3.01252522110192));
#5393=CARTESIAN_POINT('Ctrl Pts',(-0.472999999999784,-1.41823784306299,
3.01261008153856));
#5394=CARTESIAN_POINT('Ctrl Pts',(-0.473000921064235,-1.41747599318126,
3.01269480438576));
#5395=CARTESIAN_POINT('Ctrl Pts',(-0.473287797471458,-1.29873656917597,
3.02588334070707));
#5396=CARTESIAN_POINT('Ctrl Pts',(-0.497030428020275,-1.17260477262755,
3.03726209636996));
#5397=CARTESIAN_POINT('Ctrl Pts',(-0.593452559529464,-0.940241249793266,
3.05235989856664));
#5398=CARTESIAN_POINT('Ctrl Pts',(-0.666140770092878,-0.834013199901788,
3.05607990145755));
#5399=CARTESIAN_POINT('Ctrl Pts',(-0.750076984997327,-0.750076984997344,
3.05607990145755));
#5400=CARTESIAN_POINT('Ctrl Pts',(-0.834013199901775,-0.6661407700929,3.05607990145755));
#5401=CARTESIAN_POINT('Ctrl Pts',(-0.940241249793256,-0.593452559529491,
3.05235989856665));
#5402=CARTESIAN_POINT('Ctrl Pts',(-1.17260477262755,-0.497030428020314,
3.03726209636996));
#5403=CARTESIAN_POINT('Ctrl Pts',(-1.29873656917596,-0.473287797471503,
3.02588334070706));
#5404=CARTESIAN_POINT('Ctrl Pts',(-1.41747599318109,-0.473000921064287,
3.01269480438577));
#5405=CARTESIAN_POINT('Ctrl Pts',(-1.41823784306282,-0.472999999999835,
3.01261008153858));
#5406=CARTESIAN_POINT('Ctrl Pts',(-1.41899999999983,-0.472999999999835,
3.01252522110192));
#5407=CARTESIAN_POINT('',(-0.472999999999784,-1.41899999999984,1.22765307701777));
#5408=CARTESIAN_POINT('',(-0.472999999999784,-1.41899999999984,3.1));
#5409=CARTESIAN_POINT('',(-0.651395808575061,-0.866098738193354,0.27));
#5410=CARTESIAN_POINT('Origin',(-1.41899999999978,-1.41899999999983,1.22765307701777));
#5411=CARTESIAN_POINT('',(-0.866098738193358,-0.651395808575073,0.27));
#5412=CARTESIAN_POINT('Origin',(-1.41899999999978,-1.41899999999983,0.27));
#5413=CARTESIAN_POINT('',(-1.41899999999983,-0.472999999999835,1.22765307701776));
#5414=CARTESIAN_POINT('Origin',(-1.41899999999978,-1.41899999999983,1.22765307701767));
#5415=CARTESIAN_POINT('',(-1.41899999999983,-0.472999999999835,3.1));
#5416=CARTESIAN_POINT('Origin',(-0.472999999999781,-0.472999999999784,3.1));
#5417=CARTESIAN_POINT('',(-2.36767196216382,-0.472999999999886,2.87080111520185));
#5418=CARTESIAN_POINT('Origin',(2.61729806275939E-14,-0.472999999999759,
-9.73193776093083));
#5419=CARTESIAN_POINT('',(-2.24662499999997,-0.472999999999879,2.66114162663219));
#5420=CARTESIAN_POINT('Origin',(1.41899999999987,-1.41899999999979,3.1));
#5421=CARTESIAN_POINT('',(0.472999999999865,-1.41899999999981,3.01252522110192));
#5422=CARTESIAN_POINT('Ctrl Pts',(1.41899999999987,-0.472999999999785,3.01252522110192));
#5423=CARTESIAN_POINT('Ctrl Pts',(1.41823784306302,-0.472999999999785,3.01261008153856));
#5424=CARTESIAN_POINT('Ctrl Pts',(1.41747599318129,-0.473000921064237,3.01269480438575));
#5425=CARTESIAN_POINT('Ctrl Pts',(1.29873656917601,-0.473287797471458,3.02588334070706));
#5426=CARTESIAN_POINT('Ctrl Pts',(1.17260477262759,-0.497030428020274,3.03726209636996));
#5427=CARTESIAN_POINT('Ctrl Pts',(0.940241249793305,-0.59345255952946,3.05235989856664));
#5428=CARTESIAN_POINT('Ctrl Pts',(0.834013199901827,-0.666140770092873,
3.05607990145755));
#5429=CARTESIAN_POINT('Ctrl Pts',(0.750076984997382,-0.75007698499732,3.05607990145755));
#5430=CARTESIAN_POINT('Ctrl Pts',(0.666140770092937,-0.834013199901768,
3.05607990145755));
#5431=CARTESIAN_POINT('Ctrl Pts',(0.593452559529527,-0.940241249793248,
3.05235989856665));
#5432=CARTESIAN_POINT('Ctrl Pts',(0.497030428020347,-1.17260477262754,3.03726209636996));
#5433=CARTESIAN_POINT('Ctrl Pts',(0.473287797471535,-1.29873656917595,3.02588334070706));
#5434=CARTESIAN_POINT('Ctrl Pts',(0.473000921064317,-1.41747599318107,3.01269480438577));
#5435=CARTESIAN_POINT('Ctrl Pts',(0.472999999999865,-1.4182378430628,3.01261008153858));
#5436=CARTESIAN_POINT('Ctrl Pts',(0.472999999999865,-1.41899999999981,3.01252522110192));
#5437=CARTESIAN_POINT('',(0.651395808575106,-0.866098738193356,0.27));
#5438=CARTESIAN_POINT('Origin',(1.41899999999987,-1.41899999999979,0.27));
#5439=CARTESIAN_POINT('',(0.472999999999865,-1.41899999999981,1.22765307701772));
#5440=CARTESIAN_POINT('Origin',(1.41899999999987,-1.41899999999979,1.22765307701768));
#5441=CARTESIAN_POINT('',(0.472999999999865,-1.41899999999981,3.1));
#5442=CARTESIAN_POINT('Origin',(0.472999999999839,-0.472999999999785,3.1));
#5443=CARTESIAN_POINT('',(0.472999999999892,-2.36767196216382,2.87080111520185));
#5444=CARTESIAN_POINT('Origin',(0.472999999999825,1.32935445800918E-14,
-9.73193776093083));
#5445=CARTESIAN_POINT('',(0.472999999999889,-2.24662499999997,2.66114162663219));
#5446=CARTESIAN_POINT('Origin',(-2.5,0.472999999999654,3.1));
#5447=CARTESIAN_POINT('',(-2.36767196216383,0.472999999999654,2.87080111520186));
#5448=CARTESIAN_POINT('Origin',(8.32667268468867E-16,0.472999999999654,
-9.73193776093083));
#5449=CARTESIAN_POINT('',(-2.5,0.472999999999654,3.1));
#5450=CARTESIAN_POINT('Origin',(-2.5,-0.472999999999893,3.1));
#5451=CARTESIAN_POINT('',(-2.37229341204248,-2.90522153369617E-16,2.87880570119631));
#5452=CARTESIAN_POINT('Origin',(3.68139204037345,0.,-7.60648507542867));
#5453=CARTESIAN_POINT('',(-0.866098738193358,-0.236499999999945,0.27));
#5454=CARTESIAN_POINT('Origin',(3.68139204037345,0.,-7.60648507542867));
#5455=CARTESIAN_POINT('Origin',(-0.472999999999788,-2.5,3.1));
#5456=CARTESIAN_POINT('',(-0.472999999999788,-2.36767196216382,2.87080111520185));
#5457=CARTESIAN_POINT('Origin',(-0.472999999999779,1.82968396778355E-15,
-9.73193776093083));
#5458=CARTESIAN_POINT('',(-0.472999999999788,-2.5,3.1));
#5459=CARTESIAN_POINT('Origin',(0.472999999999896,-2.5,3.1));
#5460=CARTESIAN_POINT('Origin',(6.23325686399709E-15,3.68139204037346,-7.60648507542867));
#5461=CARTESIAN_POINT('',(0.236499999999949,-0.866098738193356,0.27));
#5462=CARTESIAN_POINT('Origin',(1.11022302462516E-15,3.88578058618805E-15,
0.27));
#5463=CARTESIAN_POINT('Origin',(0.,0.,-0.2));
#5464=CARTESIAN_POINT('',(2.37846096908266,-2.91277461268399E-16,-3.46944695195361E-17));
#5465=CARTESIAN_POINT('Origin',(0.,0.,-3.46944695195361E-17));
#5466=CARTESIAN_POINT('',(2.17846096908266,-2.66784525285452E-16,-0.2));
#5467=CARTESIAN_POINT('Origin',(2.37846096908266,-2.91277461268399E-16,
-0.2));
#5468=CARTESIAN_POINT('Origin',(0.,0.,-0.2));
#5469=CARTESIAN_POINT('Origin',(-2.17846096908266,0.,-1.88141750998334E-17));
#5470=CARTESIAN_POINT('',(5.15,-6.30693101560887E-16,-2.77555756156289E-16));
#5471=CARTESIAN_POINT('Origin',(0.,0.,0.));
#5472=CARTESIAN_POINT('Origin',(0.,0.,-0.149999999999999));
#5473=CARTESIAN_POINT('',(2.17846096908266,-2.66784525285452E-16,-0.299999999999998));
#5474=CARTESIAN_POINT('Origin',(0.,0.,-0.299999999999998));
#5475=CARTESIAN_POINT('',(2.17846096908266,-2.66784525285452E-16,-0.149999999999999));
#5476=CARTESIAN_POINT('Origin',(0.,0.,-0.899999999999999));
#5477=CARTESIAN_POINT('',(2.4505,-3.00099698131059E-16,-1.31526348502534));
#5478=CARTESIAN_POINT('Origin',(0.,0.,-1.31526348502534));
#5479=CARTESIAN_POINT('',(2.33923048454133,-2.86473112536145E-16,-0.899999999999999));
#5480=CARTESIAN_POINT('Origin',(0.,0.,-7.75));
#5481=CARTESIAN_POINT('',(2.4505,3.00099698131059E-16,-14.));
#5482=CARTESIAN_POINT('Origin',(0.,0.,-14.));
#5483=CARTESIAN_POINT('',(2.4505,-3.00099698131059E-16,-7.75));
#5484=CARTESIAN_POINT('Origin',(0.,0.,-14.));
#5485=CARTESIAN_POINT('Origin',(8.32667268468867E-16,0.,-9.73193776093083));
#5486=CARTESIAN_POINT('',(-4.96627380657387,0.,2.1));
#5487=CARTESIAN_POINT('Origin',(8.32667268468867E-16,0.,-9.73193776093083));
#5488=CARTESIAN_POINT('',(4.96627380657386,-6.08193132091002E-16,2.1));
#5489=CARTESIAN_POINT('Origin',(0.,0.,2.1));
#5490=CARTESIAN_POINT('Origin',(0.,0.,2.1));
#5491=CARTESIAN_POINT('Origin',(0.,0.,1.05));
#5492=CARTESIAN_POINT('',(5.05813690328693,-6.19443116825945E-16,1.05));
#7027=UNCERTAINTY_MEASURE_WITH_UNIT(LENGTH_MEASURE(0.01),#7048,
'DISTANCE_ACCURACY_VALUE',
'Maximum model space distance between geometric entities at asserted c
onnectivities');
#7035=UNCERTAINTY_MEASURE_WITH_UNIT(LENGTH_MEASURE(0.01),#7048,
'DISTANCE_ACCURACY_VALUE',
'Maximum model space distance between geometric entities at asserted c
onnectivities');
#7039=(
GEOMETRIC_REPRESENTATION_CONTEXT(3)
GLOBAL_UNCERTAINTY_ASSIGNED_CONTEXT((#7027))
GLOBAL_UNIT_ASSIGNED_CONTEXT((#7048,#7050,#7051))
REPRESENTATION_CONTEXT('','3D')
);
#7047=(
GEOMETRIC_REPRESENTATION_CONTEXT(3)
GLOBAL_UNCERTAINTY_ASSIGNED_CONTEXT((#7035))
GLOBAL_UNIT_ASSIGNED_CONTEXT((#7048,#7050,#7051))
REPRESENTATION_CONTEXT('','3D')
);
#7048=(
LENGTH_UNIT()
NAMED_UNIT(*)
SI_UNIT(.MILLI.,.METRE.)
);
#7050=(
NAMED_UNIT(*)
PLANE_ANGLE_UNIT()
SI_UNIT($,.RADIAN.)
);
#7051=(
NAMED_UNIT(*)
SI_UNIT($,.STERADIAN.)
SOLID_ANGLE_UNIT()
);
#7055=SHAPE_DEFINITION_REPRESENTATION(#7066,#7087);
#7066=PRODUCT_DEFINITION_SHAPE('',$,#7099);
#7087=SHAPE_REPRESENTATION('',(#3641),#7039);
#7095=PRODUCT_DEFINITION_CONTEXT('part definition',#7130,'design');
#7099=PRODUCT_DEFINITION('BHS JIS B 1111 - M5x14 Steel 4.6 Plain_2',
'M5x14 Steel 4.6 Plain v1 (2)',#7110,#7095);
#7110=PRODUCT_DEFINITION_FORMATION('',$,#7135);
#7130=APPLICATION_CONTEXT(
'Core Data for Automotive Mechanical Design Process');
#7131=PRODUCT_CONTEXT('part definition',#7130,'mechanical');
#7135=PRODUCT('BHS JIS B 1111 - M5x14 Steel 4.6 Plain_2',
'M5x14 Steel 4.6 Plain v1 (2)','Binding Head Screw JIS B 1111 - M5x14',
(#7131));
#7206=COLOUR_RGB('Off White',0.89,0.88,0.83);
#7207=FILL_AREA_STYLE_COLOUR('',#7206);
#7208=FILL_AREA_STYLE('',(#7207));
#7209=SURFACE_STYLE_FILL_AREA(#7208);
#7210=SURFACE_SIDE_STYLE('',(#7209));
#7211=SURFACE_STYLE_USAGE(.BOTH.,#7210);
#7212=PRESENTATION_STYLE_ASSIGNMENT((#7211));
ENDSEC;
END-ISO-10303-21;
